ISO-10303-21;
HEADER;
/* Generated by software containing ST-Developer
 * from STEP Tools, Inc. (www.steptools.com) 
 */

FILE_DESCRIPTION(
/* description */ (''),
/* implementation_level */ '2;1');

FILE_NAME(
/* name */ 'Binding Head Screw JIS B 1111 - M2x6 Steel 4.6 Plain v1 (3).step',
/* time_stamp */ '2026-10-07T02:13:48+06:00',
/* author */ (''),
/* organization */ (''),
/* preprocessor_version */ 'ST-DEVELOPER v20.2',
/* originating_system */ 'Autodesk Translation Framework v15.15.0.0',
/* authorisation */ '');

FILE_SCHEMA (('AUTOMOTIVE_DESIGN { 1 0 10303 214 3 1 1 }'));
ENDSEC;

DATA;
#10=MECHANICAL_DESIGN_GEOMETRIC_PRESENTATION_REPRESENTATION('',(#124),#17042);
#66=CONICAL_SURFACE('',#9168,0.919615242270664,0.261799387799148);
#67=CONICAL_SURFACE('',#9177,2.11281731799709,0.0872664626099693);
#100=SHAPE_REPRESENTATION_RELATIONSHIP('SRR','None',#17096,#112);
#112=ADVANCED_BREP_SHAPE_REPRESENTATION('',(#136),#17040);
#124=STYLED_ITEM('',(#17154),#136);
#136=MANIFOLD_SOLID_BREP('Body1',#8125);
#176=FACE_BOUND('',#1437,.T.);
#212=SPHERICAL_SURFACE('',#9173,6.32965591734106);
#235=TOROIDAL_SURFACE('',#9160,0.939230484541328,0.1);
#268=ELLIPSE('',#9119,0.992,0.496);
#269=ELLIPSE('',#9121,0.992,0.496);
#270=ELLIPSE('',#9126,0.992,0.496);
#271=ELLIPSE('',#9131,0.992,0.496);
#272=ELLIPSE('',#9136,0.992,0.496);
#273=ELLIPSE('',#9140,0.992,0.496);
#274=ELLIPSE('',#9142,0.992,0.496);
#275=ELLIPSE('',#9147,0.992,0.496);
#446=PLANE('',#9122);
#447=PLANE('',#9124);
#448=PLANE('',#9127);
#449=PLANE('',#9132);
#450=PLANE('',#9134);
#451=PLANE('',#9137);
#452=PLANE('',#9143);
#453=PLANE('',#9148);
#454=PLANE('',#9150);
#455=PLANE('',#9152);
#456=PLANE('',#9155);
#457=PLANE('',#9157);
#458=PLANE('',#9159);
#459=PLANE('',#9164);
#460=PLANE('',#9172);
#903=FACE_OUTER_BOUND('',#1418,.T.);
#904=FACE_OUTER_BOUND('',#1419,.T.);
#905=FACE_OUTER_BOUND('',#1420,.T.);
#906=FACE_OUTER_BOUND('',#1421,.T.);
#907=FACE_OUTER_BOUND('',#1422,.T.);
#908=FACE_OUTER_BOUND('',#1423,.T.);
#909=FACE_OUTER_BOUND('',#1424,.T.);
#910=FACE_OUTER_BOUND('',#1425,.T.);
#911=FACE_OUTER_BOUND('',#1426,.T.);
#912=FACE_OUTER_BOUND('',#1427,.T.);
#913=FACE_OUTER_BOUND('',#1428,.T.);
#914=FACE_OUTER_BOUND('',#1429,.T.);
#915=FACE_OUTER_BOUND('',#1430,.T.);
#916=FACE_OUTER_BOUND('',#1431,.T.);
#917=FACE_OUTER_BOUND('',#1432,.T.);
#918=FACE_OUTER_BOUND('',#1433,.T.);
#919=FACE_OUTER_BOUND('',#1434,.T.);
#920=FACE_OUTER_BOUND('',#1435,.T.);
#921=FACE_OUTER_BOUND('',#1436,.T.);
#922=FACE_OUTER_BOUND('',#1438,.T.);
#923=FACE_OUTER_BOUND('',#1439,.T.);
#924=FACE_OUTER_BOUND('',#1440,.T.);
#925=FACE_OUTER_BOUND('',#1441,.T.);
#926=FACE_OUTER_BOUND('',#1442,.T.);
#927=FACE_OUTER_BOUND('',#1443,.T.);
#1418=EDGE_LOOP('',(#7191,#7192,#7193,#7194,#7195,#7196));
#1419=EDGE_LOOP('',(#7197,#7198,#7199));
#1420=EDGE_LOOP('',(#7200,#7201,#7202,#7203,#7204,#7205));
#1421=EDGE_LOOP('',(#7206,#7207,#7208));
#1422=EDGE_LOOP('',(#7209,#7210,#7211,#7212,#7213,#7214));
#1423=EDGE_LOOP('',(#7215,#7216,#7217));
#1424=EDGE_LOOP('',(#7218,#7219,#7220,#7221,#7222,#7223));
#1425=EDGE_LOOP('',(#7224,#7225,#7226));
#1426=EDGE_LOOP('',(#7227,#7228,#7229,#7230,#7231,#7232));
#1427=EDGE_LOOP('',(#7233,#7234,#7235));
#1428=EDGE_LOOP('',(#7236,#7237,#7238,#7239,#7240,#7241));
#1429=EDGE_LOOP('',(#7242,#7243,#7244));
#1430=EDGE_LOOP('',(#7245,#7246,#7247));
#1431=EDGE_LOOP('',(#7248,#7249,#7250,#7251,#7252,#7253,#7254));
#1432=EDGE_LOOP('',(#7255,#7256,#7257));
#1433=EDGE_LOOP('',(#7258,#7259,#7260,#7261,#7262,#7263));
#1434=EDGE_LOOP('',(#7264,#7265,#7266,#7267,#7268,#7269,#7270,#7271));
#1435=EDGE_LOOP('',(#7272,#7273,#7274,#7275));
#1436=EDGE_LOOP('',(#7276));
#1437=EDGE_LOOP('',(#7277));
#1438=EDGE_LOOP('',(#7278,#7279,#7280,#7281));
#1439=EDGE_LOOP('',(#7282,#7283,#7284,#7285));
#1440=EDGE_LOOP('',(#7286,#7287,#7288,#7289));
#1441=EDGE_LOOP('',(#7290));
#1442=EDGE_LOOP('',(#7291,#7292,#7293,#7294,#7295,#7296,#7297,#7298,#7299,
#7300,#7301,#7302,#7303,#7304,#7305,#7306,#7307,#7308,#7309,#7310,#7311));
#1443=EDGE_LOOP('',(#7312,#7313,#7314,#7315,#7316));
#1896=CIRCLE('',#9120,0.496);
#1897=CIRCLE('',#9123,6.32479565138939);
#1898=CIRCLE('',#9125,5.93049029404341);
#1899=CIRCLE('',#9128,6.32479565138933);
#1900=CIRCLE('',#9130,0.496);
#1901=CIRCLE('',#9133,6.32479565138941);
#1902=CIRCLE('',#9135,5.93049029404341);
#1903=CIRCLE('',#9138,6.32479565138941);
#1904=CIRCLE('',#9141,0.496);
#1905=CIRCLE('',#9144,6.32479565138943);
#1906=CIRCLE('',#9146,0.496);
#1907=CIRCLE('',#9149,6.32479565138944);
#1908=CIRCLE('',#9151,6.32479565138933);
#1909=CIRCLE('',#9153,5.93049029404347);
#1910=CIRCLE('',#9154,5.93049029404347);
#1911=CIRCLE('',#9156,6.32479565138944);
#1912=CIRCLE('',#9158,5.93049029404341);
#1913=CIRCLE('',#9161,0.939230484541328);
#1914=CIRCLE('',#9162,0.1);
#1915=CIRCLE('',#9163,0.839230484541328);
#1916=CIRCLE('',#9165,2.15);
#1917=CIRCLE('',#9167,0.839230484541328);
#1918=CIRCLE('',#9169,0.96675);
#1919=CIRCLE('',#9171,0.96675);
#1920=CIRCLE('',#9174,6.32965591734106);
#1921=CIRCLE('',#9175,2.07563463599418);
#1922=CIRCLE('',#9176,2.07563463599418);
#2014=B_SPLINE_CURVE_WITH_KNOTS('',3,(#16635,#16636,#16637,#16638,#16639,
#16640,#16641,#16642,#16643,#16644,#16645,#16646,#16647,#16648,#16649),
 .UNSPECIFIED.,.F.,.F.,(4,2,2,3,2,2,4),(-0.0374758352523592,-0.0373394553501654,
-0.0186697276750827,0.,0.0186697276750831,0.0373394553501661,0.0374758352523223),
 .UNSPECIFIED.);
#2015=B_SPLINE_CURVE_WITH_KNOTS('',3,(#16677,#16678,#16679,#16680,#16681,
#16682,#16683,#16684,#16685,#16686,#16687,#16688,#16689,#16690,#16691),
 .UNSPECIFIED.,.F.,.F.,(4,2,2,3,2,2,4),(-0.0374758352523656,-0.0373394553501654,
-0.0186697276750827,0.,0.0186697276750831,0.0373394553501662,0.0374758352523289),
 .UNSPECIFIED.);
#2016=B_SPLINE_CURVE_WITH_KNOTS('',3,(#16716,#16717,#16718,#16719,#16720,
#16721,#16722,#16723,#16724,#16725,#16726,#16727,#16728,#16729,#16730),
 .UNSPECIFIED.,.F.,.F.,(4,2,2,3,2,2,4),(-0.0374758352524519,-0.0373394553501659,
-0.0186697276750829,0.,0.0186697276750829,0.0373394553501658,0.0374758352524142),
 .UNSPECIFIED.);
#2017=B_SPLINE_CURVE_WITH_KNOTS('',3,(#16746,#16747,#16748,#16749,#16750,
#16751,#16752,#16753,#16754,#16755,#16756,#16757,#16758,#16759,#16760),
 .UNSPECIFIED.,.F.,.F.,(4,2,2,3,2,2,4),(-0.0374758352524171,-0.0373394553501658,
-0.0186697276750829,0.,0.018669727675083,0.037339455350166,0.0374758352523797),
 .UNSPECIFIED.);
#2552=LINE('',#16651,#3130);
#2553=LINE('',#16658,#3131);
#2554=LINE('',#16662,#3132);
#2555=LINE('',#16667,#3133);
#2556=LINE('',#16670,#3134);
#2557=LINE('',#16674,#3135);
#2558=LINE('',#16696,#3136);
#2559=LINE('',#16700,#3137);
#2560=LINE('',#16705,#3138);
#2561=LINE('',#16708,#3139);
#2562=LINE('',#16712,#3140);
#2563=LINE('',#16732,#3141);
#2564=LINE('',#16739,#3142);
#2565=LINE('',#16743,#3143);
#2566=LINE('',#16765,#3144);
#2567=LINE('',#16769,#3145);
#2568=LINE('',#16773,#3146);
#2569=LINE('',#16777,#3147);
#2570=LINE('',#16782,#3148);
#2571=LINE('',#16785,#3149);
#2572=LINE('',#16799,#3150);
#2573=LINE('',#16803,#3151);
#2574=LINE('',#16807,#3152);
#2575=LINE('',#16816,#3153);
#3130=VECTOR('',#11499,10.);
#3131=VECTOR('',#11506,10.);
#3132=VECTOR('',#11511,10.);
#3133=VECTOR('',#11516,10.);
#3134=VECTOR('',#11519,10.);
#3135=VECTOR('',#11524,10.);
#3136=VECTOR('',#11531,10.);
#3137=VECTOR('',#11536,10.);
#3138=VECTOR('',#11541,10.);
#3139=VECTOR('',#11544,10.);
#3140=VECTOR('',#11549,10.);
#3141=VECTOR('',#11552,10.);
#3142=VECTOR('',#11559,10.);
#3143=VECTOR('',#11564,10.);
#3144=VECTOR('',#11571,10.);
#3145=VECTOR('',#11576,10.);
#3146=VECTOR('',#11581,10.);
#3147=VECTOR('',#11586,10.);
#3148=VECTOR('',#11593,10.);
#3149=VECTOR('',#11598,10.);
#3150=VECTOR('',#11617,0.839230484541328);
#3151=VECTOR('',#11622,0.919615242270664);
#3152=VECTOR('',#11627,1.);
#3153=VECTOR('',#11640,2.11281731799709);
#3830=VERTEX_POINT('',#16633);
#3831=VERTEX_POINT('',#16634);
#3832=VERTEX_POINT('',#16650);
#3833=VERTEX_POINT('',#16652);
#3834=VERTEX_POINT('',#16654);
#3835=VERTEX_POINT('',#16656);
#3836=VERTEX_POINT('',#16660);
#3837=VERTEX_POINT('',#16664);
#3838=VERTEX_POINT('',#16666);
#3839=VERTEX_POINT('',#16668);
#3840=VERTEX_POINT('',#16672);
#3841=VERTEX_POINT('',#16676);
#3842=VERTEX_POINT('',#16692);
#3843=VERTEX_POINT('',#16694);
#3844=VERTEX_POINT('',#16698);
#3845=VERTEX_POINT('',#16702);
#3846=VERTEX_POINT('',#16704);
#3847=VERTEX_POINT('',#16706);
#3848=VERTEX_POINT('',#16710);
#3849=VERTEX_POINT('',#16714);
#3850=VERTEX_POINT('',#16715);
#3851=VERTEX_POINT('',#16731);
#3852=VERTEX_POINT('',#16733);
#3853=VERTEX_POINT('',#16735);
#3854=VERTEX_POINT('',#16737);
#3855=VERTEX_POINT('',#16741);
#3856=VERTEX_POINT('',#16745);
#3857=VERTEX_POINT('',#16761);
#3858=VERTEX_POINT('',#16763);
#3859=VERTEX_POINT('',#16767);
#3860=VERTEX_POINT('',#16771);
#3861=VERTEX_POINT('',#16775);
#3862=VERTEX_POINT('',#16780);
#3863=VERTEX_POINT('',#16788);
#3864=VERTEX_POINT('',#16790);
#3865=VERTEX_POINT('',#16794);
#3866=VERTEX_POINT('',#16797);
#3867=VERTEX_POINT('',#16801);
#3868=VERTEX_POINT('',#16805);
#3869=VERTEX_POINT('',#16810);
#3870=VERTEX_POINT('',#16812);
#4963=EDGE_CURVE('',#3830,#3831,#2014,.T.);
#4964=EDGE_CURVE('',#3832,#3830,#2552,.T.);
#4965=EDGE_CURVE('',#3832,#3833,#268,.F.);
#4966=EDGE_CURVE('',#3833,#3834,#1896,.F.);
#4967=EDGE_CURVE('',#3835,#3834,#269,.T.);
#4968=EDGE_CURVE('',#3831,#3835,#2553,.T.);
#4969=EDGE_CURVE('',#3831,#3836,#1897,.T.);
#4970=EDGE_CURVE('',#3836,#3835,#2554,.F.);
#4971=EDGE_CURVE('',#3836,#3837,#1898,.T.);
#4972=EDGE_CURVE('',#3834,#3838,#2555,.F.);
#4973=EDGE_CURVE('',#3839,#3838,#270,.F.);
#4974=EDGE_CURVE('',#3837,#3839,#2556,.T.);
#4975=EDGE_CURVE('',#3837,#3840,#1899,.T.);
#4976=EDGE_CURVE('',#3839,#3840,#2557,.T.);
#4977=EDGE_CURVE('',#3840,#3841,#2015,.T.);
#4978=EDGE_CURVE('',#3838,#3842,#1900,.F.);
#4979=EDGE_CURVE('',#3843,#3842,#271,.T.);
#4980=EDGE_CURVE('',#3841,#3843,#2558,.T.);
#4981=EDGE_CURVE('',#3841,#3844,#1901,.T.);
#4982=EDGE_CURVE('',#3844,#3843,#2559,.F.);
#4983=EDGE_CURVE('',#3844,#3845,#1902,.T.);
#4984=EDGE_CURVE('',#3842,#3846,#2560,.F.);
#4985=EDGE_CURVE('',#3847,#3846,#272,.F.);
#4986=EDGE_CURVE('',#3845,#3847,#2561,.T.);
#4987=EDGE_CURVE('',#3845,#3848,#1903,.T.);
#4988=EDGE_CURVE('',#3847,#3848,#2562,.T.);
#4989=EDGE_CURVE('',#3849,#3850,#2016,.T.);
#4990=EDGE_CURVE('',#3851,#3849,#2563,.T.);
#4991=EDGE_CURVE('',#3851,#3852,#273,.F.);
#4992=EDGE_CURVE('',#3852,#3853,#1904,.F.);
#4993=EDGE_CURVE('',#3854,#3853,#274,.T.);
#4994=EDGE_CURVE('',#3850,#3854,#2564,.T.);
#4995=EDGE_CURVE('',#3850,#3855,#1905,.T.);
#4996=EDGE_CURVE('',#3855,#3854,#2565,.F.);
#4997=EDGE_CURVE('',#3848,#3856,#2017,.T.);
#4998=EDGE_CURVE('',#3846,#3857,#1906,.F.);
#4999=EDGE_CURVE('',#3858,#3857,#275,.T.);
#5000=EDGE_CURVE('',#3856,#3858,#2566,.T.);
#5001=EDGE_CURVE('',#3856,#3859,#1907,.T.);
#5002=EDGE_CURVE('',#3859,#3858,#2567,.F.);
#5003=EDGE_CURVE('',#3860,#3830,#1908,.T.);
#5004=EDGE_CURVE('',#3860,#3832,#2568,.T.);
#5005=EDGE_CURVE('',#3855,#3861,#1909,.T.);
#5006=EDGE_CURVE('',#3853,#3833,#2569,.F.);
#5007=EDGE_CURVE('',#3861,#3860,#1910,.T.);
#5008=EDGE_CURVE('',#3862,#3849,#1911,.T.);
#5009=EDGE_CURVE('',#3862,#3851,#2570,.T.);
#5010=EDGE_CURVE('',#3859,#3862,#1912,.T.);
#5011=EDGE_CURVE('',#3857,#3852,#2571,.F.);
#5012=EDGE_CURVE('',#3863,#3863,#1913,.T.);
#5013=EDGE_CURVE('',#3863,#3864,#1914,.T.);
#5014=EDGE_CURVE('',#3864,#3864,#1915,.T.);
#5015=EDGE_CURVE('',#3865,#3865,#1916,.T.);
#5016=EDGE_CURVE('',#3866,#3866,#1917,.T.);
#5017=EDGE_CURVE('',#3866,#3864,#2572,.T.);
#5018=EDGE_CURVE('',#3867,#3867,#1918,.T.);
#5019=EDGE_CURVE('',#3867,#3866,#2573,.T.);
#5020=EDGE_CURVE('',#3868,#3868,#1919,.F.);
#5021=EDGE_CURVE('',#3868,#3867,#2574,.T.);
#5022=EDGE_CURVE('',#3861,#3869,#1920,.T.);
#5023=EDGE_CURVE('',#3870,#3869,#1921,.T.);
#5024=EDGE_CURVE('',#3869,#3870,#1922,.T.);
#5025=EDGE_CURVE('',#3865,#3870,#2575,.T.);
#7191=ORIENTED_EDGE('',*,*,#4963,.F.);
#7192=ORIENTED_EDGE('',*,*,#4964,.F.);
#7193=ORIENTED_EDGE('',*,*,#4965,.T.);
#7194=ORIENTED_EDGE('',*,*,#4966,.T.);
#7195=ORIENTED_EDGE('',*,*,#4967,.F.);
#7196=ORIENTED_EDGE('',*,*,#4968,.F.);
#7197=ORIENTED_EDGE('',*,*,#4969,.F.);
#7198=ORIENTED_EDGE('',*,*,#4968,.T.);
#7199=ORIENTED_EDGE('',*,*,#4970,.F.);
#7200=ORIENTED_EDGE('',*,*,#4971,.F.);
#7201=ORIENTED_EDGE('',*,*,#4970,.T.);
#7202=ORIENTED_EDGE('',*,*,#4967,.T.);
#7203=ORIENTED_EDGE('',*,*,#4972,.T.);
#7204=ORIENTED_EDGE('',*,*,#4973,.F.);
#7205=ORIENTED_EDGE('',*,*,#4974,.F.);
#7206=ORIENTED_EDGE('',*,*,#4975,.F.);
#7207=ORIENTED_EDGE('',*,*,#4974,.T.);
#7208=ORIENTED_EDGE('',*,*,#4976,.T.);
#7209=ORIENTED_EDGE('',*,*,#4977,.F.);
#7210=ORIENTED_EDGE('',*,*,#4976,.F.);
#7211=ORIENTED_EDGE('',*,*,#4973,.T.);
#7212=ORIENTED_EDGE('',*,*,#4978,.T.);
#7213=ORIENTED_EDGE('',*,*,#4979,.F.);
#7214=ORIENTED_EDGE('',*,*,#4980,.F.);
#7215=ORIENTED_EDGE('',*,*,#4981,.F.);
#7216=ORIENTED_EDGE('',*,*,#4980,.T.);
#7217=ORIENTED_EDGE('',*,*,#4982,.F.);
#7218=ORIENTED_EDGE('',*,*,#4983,.F.);
#7219=ORIENTED_EDGE('',*,*,#4982,.T.);
#7220=ORIENTED_EDGE('',*,*,#4979,.T.);
#7221=ORIENTED_EDGE('',*,*,#4984,.T.);
#7222=ORIENTED_EDGE('',*,*,#4985,.F.);
#7223=ORIENTED_EDGE('',*,*,#4986,.F.);
#7224=ORIENTED_EDGE('',*,*,#4987,.F.);
#7225=ORIENTED_EDGE('',*,*,#4986,.T.);
#7226=ORIENTED_EDGE('',*,*,#4988,.T.);
#7227=ORIENTED_EDGE('',*,*,#4989,.F.);
#7228=ORIENTED_EDGE('',*,*,#4990,.F.);
#7229=ORIENTED_EDGE('',*,*,#4991,.T.);
#7230=ORIENTED_EDGE('',*,*,#4992,.T.);
#7231=ORIENTED_EDGE('',*,*,#4993,.F.);
#7232=ORIENTED_EDGE('',*,*,#4994,.F.);
#7233=ORIENTED_EDGE('',*,*,#4995,.F.);
#7234=ORIENTED_EDGE('',*,*,#4994,.T.);
#7235=ORIENTED_EDGE('',*,*,#4996,.F.);
#7236=ORIENTED_EDGE('',*,*,#4997,.F.);
#7237=ORIENTED_EDGE('',*,*,#4988,.F.);
#7238=ORIENTED_EDGE('',*,*,#4985,.T.);
#7239=ORIENTED_EDGE('',*,*,#4998,.T.);
#7240=ORIENTED_EDGE('',*,*,#4999,.F.);
#7241=ORIENTED_EDGE('',*,*,#5000,.F.);
#7242=ORIENTED_EDGE('',*,*,#5001,.F.);
#7243=ORIENTED_EDGE('',*,*,#5000,.T.);
#7244=ORIENTED_EDGE('',*,*,#5002,.F.);
#7245=ORIENTED_EDGE('',*,*,#5003,.F.);
#7246=ORIENTED_EDGE('',*,*,#5004,.T.);
#7247=ORIENTED_EDGE('',*,*,#4964,.T.);
#7248=ORIENTED_EDGE('',*,*,#5005,.F.);
#7249=ORIENTED_EDGE('',*,*,#4996,.T.);
#7250=ORIENTED_EDGE('',*,*,#4993,.T.);
#7251=ORIENTED_EDGE('',*,*,#5006,.T.);
#7252=ORIENTED_EDGE('',*,*,#4965,.F.);
#7253=ORIENTED_EDGE('',*,*,#5004,.F.);
#7254=ORIENTED_EDGE('',*,*,#5007,.F.);
#7255=ORIENTED_EDGE('',*,*,#5008,.F.);
#7256=ORIENTED_EDGE('',*,*,#5009,.T.);
#7257=ORIENTED_EDGE('',*,*,#4990,.T.);
#7258=ORIENTED_EDGE('',*,*,#5010,.F.);
#7259=ORIENTED_EDGE('',*,*,#5002,.T.);
#7260=ORIENTED_EDGE('',*,*,#4999,.T.);
#7261=ORIENTED_EDGE('',*,*,#5011,.T.);
#7262=ORIENTED_EDGE('',*,*,#4991,.F.);
#7263=ORIENTED_EDGE('',*,*,#5009,.F.);
#7264=ORIENTED_EDGE('',*,*,#4972,.F.);
#7265=ORIENTED_EDGE('',*,*,#4966,.F.);
#7266=ORIENTED_EDGE('',*,*,#5006,.F.);
#7267=ORIENTED_EDGE('',*,*,#4992,.F.);
#7268=ORIENTED_EDGE('',*,*,#5011,.F.);
#7269=ORIENTED_EDGE('',*,*,#4998,.F.);
#7270=ORIENTED_EDGE('',*,*,#4984,.F.);
#7271=ORIENTED_EDGE('',*,*,#4978,.F.);
#7272=ORIENTED_EDGE('',*,*,#5012,.T.);
#7273=ORIENTED_EDGE('',*,*,#5013,.T.);
#7274=ORIENTED_EDGE('',*,*,#5014,.T.);
#7275=ORIENTED_EDGE('',*,*,#5013,.F.);
#7276=ORIENTED_EDGE('',*,*,#5015,.T.);
#7277=ORIENTED_EDGE('',*,*,#5012,.F.);
#7278=ORIENTED_EDGE('',*,*,#5016,.F.);
#7279=ORIENTED_EDGE('',*,*,#5017,.T.);
#7280=ORIENTED_EDGE('',*,*,#5014,.F.);
#7281=ORIENTED_EDGE('',*,*,#5017,.F.);
#7282=ORIENTED_EDGE('',*,*,#5018,.F.);
#7283=ORIENTED_EDGE('',*,*,#5019,.T.);
#7284=ORIENTED_EDGE('',*,*,#5016,.T.);
#7285=ORIENTED_EDGE('',*,*,#5019,.F.);
#7286=ORIENTED_EDGE('',*,*,#5020,.F.);
#7287=ORIENTED_EDGE('',*,*,#5021,.T.);
#7288=ORIENTED_EDGE('',*,*,#5018,.T.);
#7289=ORIENTED_EDGE('',*,*,#5021,.F.);
#7290=ORIENTED_EDGE('',*,*,#5020,.T.);
#7291=ORIENTED_EDGE('',*,*,#4997,.T.);
#7292=ORIENTED_EDGE('',*,*,#5001,.T.);
#7293=ORIENTED_EDGE('',*,*,#5010,.T.);
#7294=ORIENTED_EDGE('',*,*,#5008,.T.);
#7295=ORIENTED_EDGE('',*,*,#4989,.T.);
#7296=ORIENTED_EDGE('',*,*,#4995,.T.);
#7297=ORIENTED_EDGE('',*,*,#5005,.T.);
#7298=ORIENTED_EDGE('',*,*,#5022,.T.);
#7299=ORIENTED_EDGE('',*,*,#5023,.F.);
#7300=ORIENTED_EDGE('',*,*,#5024,.F.);
#7301=ORIENTED_EDGE('',*,*,#5022,.F.);
#7302=ORIENTED_EDGE('',*,*,#5007,.T.);
#7303=ORIENTED_EDGE('',*,*,#5003,.T.);
#7304=ORIENTED_EDGE('',*,*,#4963,.T.);
#7305=ORIENTED_EDGE('',*,*,#4969,.T.);
#7306=ORIENTED_EDGE('',*,*,#4971,.T.);
#7307=ORIENTED_EDGE('',*,*,#4975,.T.);
#7308=ORIENTED_EDGE('',*,*,#4977,.T.);
#7309=ORIENTED_EDGE('',*,*,#4981,.T.);
#7310=ORIENTED_EDGE('',*,*,#4983,.T.);
#7311=ORIENTED_EDGE('',*,*,#4987,.T.);
#7312=ORIENTED_EDGE('',*,*,#5015,.F.);
#7313=ORIENTED_EDGE('',*,*,#5025,.T.);
#7314=ORIENTED_EDGE('',*,*,#5023,.T.);
#7315=ORIENTED_EDGE('',*,*,#5024,.T.);
#7316=ORIENTED_EDGE('',*,*,#5025,.F.);
#7626=CYLINDRICAL_SURFACE('',#9118,0.496);
#7627=CYLINDRICAL_SURFACE('',#9129,0.496);
#7628=CYLINDRICAL_SURFACE('',#9139,0.496);
#7629=CYLINDRICAL_SURFACE('',#9145,0.496);
#7630=CYLINDRICAL_SURFACE('',#9166,0.839230484541328);
#7631=CYLINDRICAL_SURFACE('',#9170,0.96675);
#8065=ADVANCED_FACE('',(#903),#7626,.T.);
#8066=ADVANCED_FACE('',(#904),#446,.F.);
#8067=ADVANCED_FACE('',(#905),#447,.F.);
#8068=ADVANCED_FACE('',(#906),#448,.F.);
#8069=ADVANCED_FACE('',(#907),#7627,.T.);
#8070=ADVANCED_FACE('',(#908),#449,.F.);
#8071=ADVANCED_FACE('',(#909),#450,.F.);
#8072=ADVANCED_FACE('',(#910),#451,.F.);
#8073=ADVANCED_FACE('',(#911),#7628,.T.);
#8074=ADVANCED_FACE('',(#912),#452,.F.);
#8075=ADVANCED_FACE('',(#913),#7629,.T.);
#8076=ADVANCED_FACE('',(#914),#453,.F.);
#8077=ADVANCED_FACE('',(#915),#454,.F.);
#8078=ADVANCED_FACE('',(#916),#455,.F.);
#8079=ADVANCED_FACE('',(#917),#456,.F.);
#8080=ADVANCED_FACE('',(#918),#457,.F.);
#8081=ADVANCED_FACE('',(#919),#458,.F.);
#8082=ADVANCED_FACE('',(#920),#235,.F.);
#8083=ADVANCED_FACE('',(#921,#176),#459,.T.);
#8084=ADVANCED_FACE('',(#922),#7630,.T.);
#8085=ADVANCED_FACE('',(#923),#66,.T.);
#8086=ADVANCED_FACE('',(#924),#7631,.T.);
#8087=ADVANCED_FACE('',(#925),#460,.T.);
#8088=ADVANCED_FACE('',(#926),#212,.T.);
#8089=ADVANCED_FACE('',(#927),#67,.T.);
#8125=CLOSED_SHELL('',(#8065,#8066,#8067,#8068,#8069,#8070,#8071,#8072,
#8073,#8074,#8075,#8076,#8077,#8078,#8079,#8080,#8081,#8082,#8083,#8084,
#8085,#8086,#8087,#8088,#8089));
#9117=AXIS2_PLACEMENT_3D('',#16631,#11495,#11496);
#9118=AXIS2_PLACEMENT_3D('',#16632,#11497,#11498);
#9119=AXIS2_PLACEMENT_3D('',#16653,#11500,#11501);
#9120=AXIS2_PLACEMENT_3D('',#16655,#11502,#11503);
#9121=AXIS2_PLACEMENT_3D('',#16657,#11504,#11505);
#9122=AXIS2_PLACEMENT_3D('',#16659,#11507,#11508);
#9123=AXIS2_PLACEMENT_3D('',#16661,#11509,#11510);
#9124=AXIS2_PLACEMENT_3D('',#16663,#11512,#11513);
#9125=AXIS2_PLACEMENT_3D('',#16665,#11514,#11515);
#9126=AXIS2_PLACEMENT_3D('',#16669,#11517,#11518);
#9127=AXIS2_PLACEMENT_3D('',#16671,#11520,#11521);
#9128=AXIS2_PLACEMENT_3D('',#16673,#11522,#11523);
#9129=AXIS2_PLACEMENT_3D('',#16675,#11525,#11526);
#9130=AXIS2_PLACEMENT_3D('',#16693,#11527,#11528);
#9131=AXIS2_PLACEMENT_3D('',#16695,#11529,#11530);
#9132=AXIS2_PLACEMENT_3D('',#16697,#11532,#11533);
#9133=AXIS2_PLACEMENT_3D('',#16699,#11534,#11535);
#9134=AXIS2_PLACEMENT_3D('',#16701,#11537,#11538);
#9135=AXIS2_PLACEMENT_3D('',#16703,#11539,#11540);
#9136=AXIS2_PLACEMENT_3D('',#16707,#11542,#11543);
#9137=AXIS2_PLACEMENT_3D('',#16709,#11545,#11546);
#9138=AXIS2_PLACEMENT_3D('',#16711,#11547,#11548);
#9139=AXIS2_PLACEMENT_3D('',#16713,#11550,#11551);
#9140=AXIS2_PLACEMENT_3D('',#16734,#11553,#11554);
#9141=AXIS2_PLACEMENT_3D('',#16736,#11555,#11556);
#9142=AXIS2_PLACEMENT_3D('',#16738,#11557,#11558);
#9143=AXIS2_PLACEMENT_3D('',#16740,#11560,#11561);
#9144=AXIS2_PLACEMENT_3D('',#16742,#11562,#11563);
#9145=AXIS2_PLACEMENT_3D('',#16744,#11565,#11566);
#9146=AXIS2_PLACEMENT_3D('',#16762,#11567,#11568);
#9147=AXIS2_PLACEMENT_3D('',#16764,#11569,#11570);
#9148=AXIS2_PLACEMENT_3D('',#16766,#11572,#11573);
#9149=AXIS2_PLACEMENT_3D('',#16768,#11574,#11575);
#9150=AXIS2_PLACEMENT_3D('',#16770,#11577,#11578);
#9151=AXIS2_PLACEMENT_3D('',#16772,#11579,#11580);
#9152=AXIS2_PLACEMENT_3D('',#16774,#11582,#11583);
#9153=AXIS2_PLACEMENT_3D('',#16776,#11584,#11585);
#9154=AXIS2_PLACEMENT_3D('',#16778,#11587,#11588);
#9155=AXIS2_PLACEMENT_3D('',#16779,#11589,#11590);
#9156=AXIS2_PLACEMENT_3D('',#16781,#11591,#11592);
#9157=AXIS2_PLACEMENT_3D('',#16783,#11594,#11595);
#9158=AXIS2_PLACEMENT_3D('',#16784,#11596,#11597);
#9159=AXIS2_PLACEMENT_3D('',#16786,#11599,#11600);
#9160=AXIS2_PLACEMENT_3D('',#16787,#11601,#11602);
#9161=AXIS2_PLACEMENT_3D('',#16789,#11603,#11604);
#9162=AXIS2_PLACEMENT_3D('',#16791,#11605,#11606);
#9163=AXIS2_PLACEMENT_3D('',#16792,#11607,#11608);
#9164=AXIS2_PLACEMENT_3D('',#16793,#11609,#11610);
#9165=AXIS2_PLACEMENT_3D('',#16795,#11611,#11612);
#9166=AXIS2_PLACEMENT_3D('',#16796,#11613,#11614);
#9167=AXIS2_PLACEMENT_3D('',#16798,#11615,#11616);
#9168=AXIS2_PLACEMENT_3D('',#16800,#11618,#11619);
#9169=AXIS2_PLACEMENT_3D('',#16802,#11620,#11621);
#9170=AXIS2_PLACEMENT_3D('',#16804,#11623,#11624);
#9171=AXIS2_PLACEMENT_3D('',#16806,#11625,#11626);
#9172=AXIS2_PLACEMENT_3D('',#16808,#11628,#11629);
#9173=AXIS2_PLACEMENT_3D('',#16809,#11630,#11631);
#9174=AXIS2_PLACEMENT_3D('',#16811,#11632,#11633);
#9175=AXIS2_PLACEMENT_3D('',#16813,#11634,#11635);
#9176=AXIS2_PLACEMENT_3D('',#16814,#11636,#11637);
#9177=AXIS2_PLACEMENT_3D('',#16815,#11638,#11639);
#11495=DIRECTION('axis',(0.,0.,1.));
#11496=DIRECTION('refdir',(1.,0.,0.));
#11497=DIRECTION('center_axis',(0.,0.,-1.));
#11498=DIRECTION('ref_axis',(0.707106781186864,-0.707106781186231,0.));
#11499=DIRECTION('',(0.,0.,1.));
#11500=DIRECTION('center_axis',(-0.866025403784439,2.42308806056559E-16,
-0.5));
#11501=DIRECTION('ref_axis',(0.5,-1.39897054514259E-16,-0.866025403784439));
#11502=DIRECTION('center_axis',(0.,0.,-1.));
#11503=DIRECTION('ref_axis',(0.707106781186864,-0.707106781186231,0.));
#11504=DIRECTION('center_axis',(-1.34432925600244E-12,0.866025403784439,
-0.5));
#11505=DIRECTION('ref_axis',(7.76183832708735E-13,-0.5,-0.866025403784439));
#11506=DIRECTION('',(0.,0.,-1.));
#11507=DIRECTION('center_axis',(-1.,-8.96558844583498E-13,0.));
#11508=DIRECTION('ref_axis',(-8.96558844583498E-13,1.,0.));
#11509=DIRECTION('center_axis',(-1.,-8.96558844583498E-13,0.));
#11510=DIRECTION('ref_axis',(0.,0.,-1.));
#11511=DIRECTION('',(-4.48279422291749E-13,0.5,0.866025403784439));
#11512=DIRECTION('center_axis',(-1.34432925600244E-12,0.866025403784439,
-0.5));
#11513=DIRECTION('ref_axis',(1.,1.55229771566499E-12,0.));
#11514=DIRECTION('center_axis',(-1.34432925600244E-12,0.866025403784439,
-0.5));
#11515=DIRECTION('ref_axis',(0.,-0.5,-0.866025403784439));
#11516=DIRECTION('',(-1.,-1.55229771566499E-12,0.));
#11517=DIRECTION('center_axis',(-1.34432925600244E-12,0.866025403784439,
-0.5));
#11518=DIRECTION('ref_axis',(7.76183832708735E-13,-0.5,-0.866025403784439));
#11519=DIRECTION('',(7.28095205575773E-14,-0.5,-0.866025403784439));
#11520=DIRECTION('center_axis',(1.,1.45619041115155E-13,0.));
#11521=DIRECTION('ref_axis',(1.45619041115155E-13,-1.,0.));
#11522=DIRECTION('center_axis',(1.,1.45619041115155E-13,0.));
#11523=DIRECTION('ref_axis',(0.,0.,1.));
#11524=DIRECTION('',(0.,0.,1.));
#11525=DIRECTION('center_axis',(0.,0.,-1.));
#11526=DIRECTION('ref_axis',(-0.707106781186035,-0.70710678118706,0.));
#11527=DIRECTION('center_axis',(0.,0.,-1.));
#11528=DIRECTION('ref_axis',(-0.707106781186035,-0.70710678118706,0.));
#11529=DIRECTION('center_axis',(0.866025403784439,1.82700839766916E-13,
-0.5));
#11530=DIRECTION('ref_axis',(-0.5,-1.0551735336738E-13,-0.866025403784439));
#11531=DIRECTION('',(0.,0.,-1.));
#11532=DIRECTION('center_axis',(-1.30466679482154E-12,1.,0.));
#11533=DIRECTION('ref_axis',(1.,1.30466679482154E-12,0.));
#11534=DIRECTION('center_axis',(-1.30466679482154E-12,1.,0.));
#11535=DIRECTION('ref_axis',(0.,0.,-1.));
#11536=DIRECTION('',(0.5,6.52333397410772E-13,0.866025403784439));
#11537=DIRECTION('center_axis',(0.866025403784439,1.82700839766916E-13,
-0.5));
#11538=DIRECTION('ref_axis',(2.10964758041199E-13,-1.,0.));
#11539=DIRECTION('center_axis',(0.866025403784439,1.82700839766916E-13,
-0.5));
#11540=DIRECTION('ref_axis',(0.5,0.,0.866025403784439));
#11541=DIRECTION('',(-2.10964758041199E-13,1.,0.));
#11542=DIRECTION('center_axis',(0.866025403784439,1.82700839766916E-13,
-0.5));
#11543=DIRECTION('ref_axis',(-0.5,-1.05482379103751E-13,-0.866025403784439));
#11544=DIRECTION('',(-0.5,6.4832235838889E-13,-0.866025403784439));
#11545=DIRECTION('center_axis',(-1.29664471677778E-12,-1.,0.));
#11546=DIRECTION('ref_axis',(-1.,1.29664471677778E-12,0.));
#11547=DIRECTION('center_axis',(-1.29664471677778E-12,-1.,0.));
#11548=DIRECTION('ref_axis',(0.,0.,1.));
#11549=DIRECTION('',(0.,0.,1.));
#11550=DIRECTION('center_axis',(0.,0.,-1.));
#11551=DIRECTION('ref_axis',(0.707106781186895,0.7071067811862,0.));
#11552=DIRECTION('',(0.,0.,1.));
#11553=DIRECTION('center_axis',(-1.35644469630397E-12,-0.866025403784439,
-0.5));
#11554=DIRECTION('ref_axis',(7.8314371117082E-13,0.5,-0.866025403784439));
#11555=DIRECTION('center_axis',(0.,0.,-1.));
#11556=DIRECTION('ref_axis',(0.707106781186895,0.7071067811862,0.));
#11557=DIRECTION('center_axis',(-0.866025403784439,2.42308806056559E-16,
-0.5));
#11558=DIRECTION('ref_axis',(0.5,-1.39897054514259E-16,-0.866025403784439));
#11559=DIRECTION('',(0.,0.,-1.));
#11560=DIRECTION('center_axis',(1.80920256647203E-12,-1.,0.));
#11561=DIRECTION('ref_axis',(-1.,-1.80920256647203E-12,0.));
#11562=DIRECTION('center_axis',(1.80920256647203E-12,-1.,0.));
#11563=DIRECTION('ref_axis',(0.,0.,1.));
#11564=DIRECTION('',(-0.5,-9.04601283236015E-13,0.866025403784439));
#11565=DIRECTION('center_axis',(0.,0.,-1.));
#11566=DIRECTION('ref_axis',(-0.707106781186768,0.707106781186327,0.));
#11567=DIRECTION('center_axis',(0.,0.,-1.));
#11568=DIRECTION('ref_axis',(-0.707106781186768,0.707106781186327,0.));
#11569=DIRECTION('center_axis',(-1.35644469630397E-12,-0.866025403784439,
-0.5));
#11570=DIRECTION('ref_axis',(7.83108736907191E-13,0.5,-0.866025403784439));
#11571=DIRECTION('',(0.,0.,-1.));
#11572=DIRECTION('center_axis',(1.,1.91935343509834E-12,0.));
#11573=DIRECTION('ref_axis',(1.91935343509834E-12,-1.,0.));
#11574=DIRECTION('center_axis',(1.,1.91935343509834E-12,0.));
#11575=DIRECTION('ref_axis',(0.,0.,1.));
#11576=DIRECTION('',(9.59676717549172E-13,-0.5,0.866025403784439));
#11577=DIRECTION('center_axis',(-1.62884833462111E-16,1.,0.));
#11578=DIRECTION('ref_axis',(1.,1.62884833462111E-16,0.));
#11579=DIRECTION('center_axis',(-1.62884833462111E-16,1.,0.));
#11580=DIRECTION('ref_axis',(0.,0.,-1.));
#11581=DIRECTION('',(0.5,8.14424167310554E-17,-0.866025403784439));
#11582=DIRECTION('center_axis',(-0.866025403784439,2.42308806056559E-16,
-0.5));
#11583=DIRECTION('ref_axis',(2.79794108807543E-16,1.,0.));
#11584=DIRECTION('center_axis',(-0.866025403784439,2.42308806056559E-16,
-0.5));
#11585=DIRECTION('ref_axis',(0.5,0.,-0.866025403784439));
#11586=DIRECTION('',(-2.79794108807543E-16,-1.,0.));
#11587=DIRECTION('center_axis',(-0.866025403784439,2.42308806056559E-16,
-0.5));
#11588=DIRECTION('ref_axis',(0.5,0.,-0.866025403784439));
#11589=DIRECTION('center_axis',(-1.,2.79168316070879E-12,0.));
#11590=DIRECTION('ref_axis',(2.79168316070879E-12,1.,0.));
#11591=DIRECTION('center_axis',(-1.,2.79168316070879E-12,0.));
#11592=DIRECTION('ref_axis',(0.,0.,-1.));
#11593=DIRECTION('',(1.3958415803544E-12,0.5,-0.866025403784439));
#11594=DIRECTION('center_axis',(-1.35644469630397E-12,-0.866025403784439,
-0.5));
#11595=DIRECTION('ref_axis',(-1.,1.56628742110387E-12,0.));
#11596=DIRECTION('center_axis',(-1.35644469630397E-12,-0.866025403784439,
-0.5));
#11597=DIRECTION('ref_axis',(0.,-0.5,0.866025403784439));
#11598=DIRECTION('',(1.,-1.56628742110387E-12,0.));
#11599=DIRECTION('center_axis',(0.,0.,-1.));
#11600=DIRECTION('ref_axis',(-1.,0.,0.));
#11601=DIRECTION('center_axis',(0.,0.,-1.));
#11602=DIRECTION('ref_axis',(-1.,0.,0.));
#11603=DIRECTION('center_axis',(0.,0.,-1.));
#11604=DIRECTION('ref_axis',(1.,0.,0.));
#11605=DIRECTION('center_axis',(-1.22464679914735E-16,-1.,0.));
#11606=DIRECTION('ref_axis',(1.,-1.22464679914735E-16,0.));
#11607=DIRECTION('center_axis',(0.,0.,1.));
#11608=DIRECTION('ref_axis',(1.,0.,0.));
#11609=DIRECTION('center_axis',(0.,0.,-1.));
#11610=DIRECTION('ref_axis',(-1.,0.,0.));
#11611=DIRECTION('center_axis',(0.,0.,-1.));
#11612=DIRECTION('ref_axis',(1.,0.,0.));
#11613=DIRECTION('center_axis',(0.,0.,-1.));
#11614=DIRECTION('ref_axis',(-1.,0.,0.));
#11615=DIRECTION('center_axis',(0.,0.,-1.));
#11616=DIRECTION('ref_axis',(1.,0.,0.));
#11617=DIRECTION('',(0.,0.,1.));
#11618=DIRECTION('center_axis',(0.,0.,-1.));
#11619=DIRECTION('ref_axis',(-1.,0.,0.));
#11620=DIRECTION('center_axis',(0.,0.,-1.));
#11621=DIRECTION('ref_axis',(-1.,0.,0.));
#11622=DIRECTION('',(-0.258819045102519,3.16961915143174E-17,0.965925826289069));
#11623=DIRECTION('center_axis',(0.,0.,-1.));
#11624=DIRECTION('ref_axis',(-1.,0.,0.));
#11625=DIRECTION('center_axis',(0.,0.,1.));
#11626=DIRECTION('ref_axis',(-1.,0.,0.));
#11627=DIRECTION('',(0.,0.,1.));
#11628=DIRECTION('center_axis',(0.,0.,-1.));
#11629=DIRECTION('ref_axis',(-1.,0.,0.));
#11630=DIRECTION('center_axis',(6.12323399573676E-17,0.,1.));
#11631=DIRECTION('ref_axis',(1.,0.,0.));
#11632=DIRECTION('center_axis',(1.22464679914735E-16,-1.,0.));
#11633=DIRECTION('ref_axis',(-1.,-1.22464679914735E-16,0.));
#11634=DIRECTION('center_axis',(0.,0.,-1.));
#11635=DIRECTION('ref_axis',(1.,0.,0.));
#11636=DIRECTION('center_axis',(0.,0.,-1.));
#11637=DIRECTION('ref_axis',(1.,0.,0.));
#11638=DIRECTION('center_axis',(0.,0.,-1.));
#11639=DIRECTION('ref_axis',(-1.,0.,0.));
#11640=DIRECTION('',(-0.087155742757872,1.06735001395738E-17,0.996194698090852));
#16631=CARTESIAN_POINT('',(0.,0.,0.));
#16632=CARTESIAN_POINT('Origin',(-0.744000000195138,0.744000000196221,1.2));
#16633=CARTESIAN_POINT('',(-0.744000000195138,0.248000000196221,1.15122809938326));
#16634=CARTESIAN_POINT('',(-0.248000000195138,0.744000000196666,1.15122809938313));
#16635=CARTESIAN_POINT('Ctrl Pts',(-0.744000000195138,0.248000000196221,
1.15122809938326));
#16636=CARTESIAN_POINT('Ctrl Pts',(-0.743548129195526,0.248000000196221,
1.15128162561029));
#16637=CARTESIAN_POINT('Ctrl Pts',(-0.743096462399636,0.248000617700407,
1.15133505381795));
#16638=CARTESIAN_POINT('Ctrl Pts',(-0.68084251616827,0.248170686680912,
1.1586889909138));
#16639=CARTESIAN_POINT('Ctrl Pts',(-0.614748859330863,0.260619583354249,
1.16502989619583));
#16640=CARTESIAN_POINT('Ctrl Pts',(-0.492966510303847,0.311166686726808,
1.17344391775669));
#16641=CARTESIAN_POINT('Ctrl Pts',(-0.437280006866291,0.349270066587974,
1.17551763482271));
#16642=CARTESIAN_POINT('Ctrl Pts',(-0.393275036726453,0.393275036727851,
1.17551763482269));
#16643=CARTESIAN_POINT('Ctrl Pts',(-0.349270066586615,0.437280006867729,
1.17551763482268));
#16644=CARTESIAN_POINT('Ctrl Pts',(-0.3111666867255,0.49296651030532,1.17344391775664));
#16645=CARTESIAN_POINT('Ctrl Pts',(-0.26061958335305,0.61474885933238,1.16502989619573));
#16646=CARTESIAN_POINT('Ctrl Pts',(-0.248170686679772,0.680842516169798,
1.15868899091368));
#16647=CARTESIAN_POINT('Ctrl Pts',(-0.248000617699323,0.743096462401038,
1.15133505381783));
#16648=CARTESIAN_POINT('Ctrl Pts',(-0.248000000195138,0.743548129196929,
1.15128162561017));
#16649=CARTESIAN_POINT('Ctrl Pts',(-0.248000000195138,0.744000000196666,
1.15122809938313));
#16650=CARTESIAN_POINT('',(-0.744000000195138,0.248000000196221,0.583389912843141));
#16651=CARTESIAN_POINT('',(-0.744000000195138,0.248000000196221,1.2));
#16652=CARTESIAN_POINT('',(-0.516876228118667,0.303056928861888,0.19));
#16653=CARTESIAN_POINT('Origin',(-0.744000000195138,0.744000000196221,0.583389912843142));
#16654=CARTESIAN_POINT('',(-0.303056928861701,0.51687622811801,0.19));
#16655=CARTESIAN_POINT('Origin',(-0.744000000195138,0.744000000196221,0.19));
#16656=CARTESIAN_POINT('',(-0.248000000195138,0.744000000196666,0.583389912846777));
#16657=CARTESIAN_POINT('Origin',(-0.744000000195138,0.744000000196221,0.583389912847341));
#16658=CARTESIAN_POINT('',(-0.248000000195138,0.744000000196666,1.2));
#16659=CARTESIAN_POINT('Origin',(-0.248000000194694,0.24800000019315,1.2));
#16660=CARTESIAN_POINT('',(-0.24800000019541,1.04682989872245,1.10790668314437));
#16661=CARTESIAN_POINT('Origin',(-0.248000000194471,-2.22346593631069E-13,
-5.12965591734105));
#16662=CARTESIAN_POINT('',(-0.248000000195362,0.993500000023809,1.01553658903582));
#16663=CARTESIAN_POINT('Origin',(-0.248000000195457,1.09999999999962,1.2));
#16664=CARTESIAN_POINT('',(0.248000000196041,1.04682989872314,1.10790668314423));
#16665=CARTESIAN_POINT('Origin',(2.9811416492917E-12,-1.91582141081592,
-4.02355591008723));
#16666=CARTESIAN_POINT('',(0.303056928861511,0.516876228118951,0.19));
#16667=CARTESIAN_POINT('',(-0.124000000097707,0.516876228118288,0.19));
#16668=CARTESIAN_POINT('',(0.248000000196085,0.744000000194883,0.583389912842355));
#16669=CARTESIAN_POINT('Origin',(0.744000000196085,0.744000000194955,0.583389912841147));
#16670=CARTESIAN_POINT('',(0.248000000196033,1.1000000000003,1.19999999999985));
#16671=CARTESIAN_POINT('Origin',(0.248000000196033,1.10000000000039,1.2));
#16672=CARTESIAN_POINT('',(0.248000000196085,0.744000000194883,1.1512280993833));
#16673=CARTESIAN_POINT('Origin',(0.248000000196193,3.61135222251268E-14,
-5.12965591734105));
#16674=CARTESIAN_POINT('',(0.248000000196085,0.744000000194883,1.2));
#16675=CARTESIAN_POINT('Origin',(0.744000000196085,0.744000000194955,1.2));
#16676=CARTESIAN_POINT('',(0.744000000196732,0.248000000194955,1.15122809938313));
#16677=CARTESIAN_POINT('Ctrl Pts',(0.248000000196085,0.744000000194883,
1.1512280993833));
#16678=CARTESIAN_POINT('Ctrl Pts',(0.248000000196085,0.743548129195249,
1.15128162561033));
#16679=CARTESIAN_POINT('Ctrl Pts',(0.24800061770027,0.743096462399337,1.15133505381799));
#16680=CARTESIAN_POINT('Ctrl Pts',(0.248170686680793,0.68084251616795,1.15868899091384));
#16681=CARTESIAN_POINT('Ctrl Pts',(0.260619583354148,0.614748859330546,
1.16502989619587));
#16682=CARTESIAN_POINT('Ctrl Pts',(0.311166686726741,0.492966510303544,
1.17344391775672));
#16683=CARTESIAN_POINT('Ctrl Pts',(0.349270066587923,0.437280006865998,
1.17551763482273));
#16684=CARTESIAN_POINT('Ctrl Pts',(0.393275036727812,0.393275036726173,
1.17551763482271));
#16685=CARTESIAN_POINT('Ctrl Pts',(0.437280006867702,0.349270066586347,
1.1755176348227));
#16686=CARTESIAN_POINT('Ctrl Pts',(0.492966510305304,0.311166686725247,
1.17344391775665));
#16687=CARTESIAN_POINT('Ctrl Pts',(0.614748859332378,0.26061958335283,1.16502989619575));
#16688=CARTESIAN_POINT('Ctrl Pts',(0.6808425161698,0.248170686679572,1.15868899091369));
#16689=CARTESIAN_POINT('Ctrl Pts',(0.743096462401062,0.24800061769914,1.15133505381783));
#16690=CARTESIAN_POINT('Ctrl Pts',(0.743548129196974,0.248000000194955,
1.15128162561017));
#16691=CARTESIAN_POINT('Ctrl Pts',(0.744000000196732,0.248000000194955,
1.15122809938313));
#16692=CARTESIAN_POINT('',(0.516876228118432,0.30305692886123,0.19));
#16693=CARTESIAN_POINT('Origin',(0.744000000196085,0.744000000194955,0.19));
#16694=CARTESIAN_POINT('',(0.744000000196732,0.248000000194955,0.583389912846289));
#16695=CARTESIAN_POINT('Origin',(0.744000000196085,0.744000000194955,0.583389912845349));
#16696=CARTESIAN_POINT('',(0.744000000196732,0.248000000194955,1.2));
#16697=CARTESIAN_POINT('Origin',(0.248000000196157,0.248000000194308,1.2));
#16698=CARTESIAN_POINT('',(1.04682989872277,0.24800000019535,1.10790668314432));
#16699=CARTESIAN_POINT('Origin',(-3.16340915708764E-13,0.248000000193984,
-5.12965591734105));
#16700=CARTESIAN_POINT('',(0.99350000002449,0.248000000195281,1.01553658903639));
#16701=CARTESIAN_POINT('Origin',(1.09999999999997,0.248000000195419,1.2));
#16702=CARTESIAN_POINT('',(1.04682989872287,-0.248000000195507,1.1079066831443));
#16703=CARTESIAN_POINT('Origin',(-1.91582141081591,-4.04170800382928E-13,
-4.02355591008723));
#16704=CARTESIAN_POINT('',(0.51687622811856,-0.3030569288607,0.19));
#16705=CARTESIAN_POINT('',(0.51687622811847,0.124000000097702,0.19));
#16706=CARTESIAN_POINT('',(0.744000000195517,-0.248000000195115,0.583389912844004));
#16707=CARTESIAN_POINT('Origin',(0.744000000194874,-0.744000000195115,0.583389912842708));
#16708=CARTESIAN_POINT('',(1.09999999999998,-0.248000000195576,1.19999999999984));
#16709=CARTESIAN_POINT('Origin',(1.10000000000007,-0.248000000195576,1.2));
#16710=CARTESIAN_POINT('',(0.744000000195517,-0.248000000195115,1.15122809938326));
#16711=CARTESIAN_POINT('Origin',(-3.14351440352569E-13,-0.24800000019415,
-5.12965591734105));
#16712=CARTESIAN_POINT('',(0.744000000195517,-0.248000000195115,1.2));
#16713=CARTESIAN_POINT('Origin',(-0.744000000195415,-0.744000000194864,
1.2));
#16714=CARTESIAN_POINT('',(-0.248000000195415,-0.744000000196249,1.15122809938316));
#16715=CARTESIAN_POINT('',(-0.744000000196312,-0.248000000194864,1.15122809938318));
#16716=CARTESIAN_POINT('Ctrl Pts',(-0.248000000195415,-0.744000000196249,
1.15122809938316));
#16717=CARTESIAN_POINT('Ctrl Pts',(-0.248000000195414,-0.74354812919633,
1.15128162561023));
#16718=CARTESIAN_POINT('Ctrl Pts',(-0.248000617699598,-0.743096462400134,
1.15133505381792));
#16719=CARTESIAN_POINT('Ctrl Pts',(-0.248170686680046,-0.680842516168463,
1.15868899091381));
#16720=CARTESIAN_POINT('Ctrl Pts',(-0.260619583353321,-0.614748859331044,
1.16502989619585));
#16721=CARTESIAN_POINT('Ctrl Pts',(-0.311166686725766,-0.49296651030398,
1.17344391775673));
#16722=CARTESIAN_POINT('Ctrl Pts',(-0.349270066586879,-0.437280006866388,
1.17551763482276));
#16723=CARTESIAN_POINT('Ctrl Pts',(-0.393275036726715,-0.393275036726509,
1.17551763482276));
#16724=CARTESIAN_POINT('Ctrl Pts',(-0.437280006866551,-0.349270066586629,
1.17551763482276));
#16725=CARTESIAN_POINT('Ctrl Pts',(-0.492966510304106,-0.311166686725461,
1.17344391775673));
#16726=CARTESIAN_POINT('Ctrl Pts',(-0.61474885933112,-0.260619583352896,
1.16502989619586));
#16727=CARTESIAN_POINT('Ctrl Pts',(-0.680842516168527,-0.248170686679557,
1.15868899091382));
#16728=CARTESIAN_POINT('Ctrl Pts',(-0.743096462400073,-0.248000617699049,
1.15133505381795));
#16729=CARTESIAN_POINT('Ctrl Pts',(-0.74354812919627,-0.248000000194863,
1.15128162561025));
#16730=CARTESIAN_POINT('Ctrl Pts',(-0.744000000196312,-0.248000000194864,
1.15122809938318));
#16731=CARTESIAN_POINT('',(-0.248000000195415,-0.744000000196249,0.58338991284606));
#16732=CARTESIAN_POINT('',(-0.248000000195415,-0.744000000196249,1.2));
#16733=CARTESIAN_POINT('',(-0.303056928861281,-0.516876228118006,0.19));
#16734=CARTESIAN_POINT('Origin',(-0.744000000195415,-0.744000000194864,
0.583389912845007));
#16735=CARTESIAN_POINT('',(-0.516876228118667,-0.303056928860673,0.19));
#16736=CARTESIAN_POINT('Origin',(-0.744000000195415,-0.744000000194864,
0.19));
#16737=CARTESIAN_POINT('',(-0.744000000196312,-0.248000000194864,0.583389912845176));
#16738=CARTESIAN_POINT('Origin',(-0.744000000195415,-0.744000000194864,
0.583389912843621));
#16739=CARTESIAN_POINT('',(-0.744000000196312,-0.248000000194864,1.2));
#16740=CARTESIAN_POINT('Origin',(-0.24800000019403,-0.248000000193966,1.2));
#16741=CARTESIAN_POINT('',(-1.04682989872298,-0.248000000195412,1.10790668314428));
#16742=CARTESIAN_POINT('Origin',(4.5589868649524E-13,-0.248000000193518,
-5.12965591734105));
#16743=CARTESIAN_POINT('',(-0.993500000024419,-0.248000000195315,1.01553658903588));
#16744=CARTESIAN_POINT('Origin',(0.744000000194874,-0.744000000195115,1.2));
#16745=CARTESIAN_POINT('',(0.248000000194874,-0.744000000196067,1.15122809938321));
#16746=CARTESIAN_POINT('Ctrl Pts',(0.744000000195517,-0.248000000195115,
1.15122809938326));
#16747=CARTESIAN_POINT('Ctrl Pts',(0.743548129195714,-0.248000000195114,
1.15128162561031));
#16748=CARTESIAN_POINT('Ctrl Pts',(0.743096462399633,-0.248000617699299,
1.15133505381799));
#16749=CARTESIAN_POINT('Ctrl Pts',(0.680842516168076,-0.248170686679796,
1.15868899091386));
#16750=CARTESIAN_POINT('Ctrl Pts',(0.614748859330666,-0.260619583353124,
1.1650298961959));
#16751=CARTESIAN_POINT('Ctrl Pts',(0.492966510303643,-0.311166686725667,
1.17344391775676));
#16752=CARTESIAN_POINT('Ctrl Pts',(0.437280006866081,-0.349270066586825,
1.17551763482279));
#16753=CARTESIAN_POINT('Ctrl Pts',(0.393275036726237,-0.393275036726696,
1.17551763482278));
#16754=CARTESIAN_POINT('Ctrl Pts',(0.349270066586393,-0.437280006866568,
1.17551763482278));
#16755=CARTESIAN_POINT('Ctrl Pts',(0.31116668672527,-0.492966510304154,
1.17344391775674));
#16756=CARTESIAN_POINT('Ctrl Pts',(0.260619583352803,-0.614748859331208,
1.16502989619586));
#16757=CARTESIAN_POINT('Ctrl Pts',(0.248170686679517,-0.680842516168625,
1.15868899091381));
#16758=CARTESIAN_POINT('Ctrl Pts',(0.248000617699059,-0.743096462400057,
1.15133505381795));
#16759=CARTESIAN_POINT('Ctrl Pts',(0.248000000194873,-0.743548129196139,
1.15128162561027));
#16760=CARTESIAN_POINT('Ctrl Pts',(0.248000000194874,-0.744000000196067,
1.15122809938321));
#16761=CARTESIAN_POINT('',(0.30305692886038,-0.516876228118955,0.19));
#16762=CARTESIAN_POINT('Origin',(0.744000000194874,-0.744000000195115,0.19));
#16763=CARTESIAN_POINT('',(0.248000000194874,-0.744000000196067,0.5833899128444));
#16764=CARTESIAN_POINT('Origin',(0.744000000194874,-0.744000000195115,0.583389912841405));
#16765=CARTESIAN_POINT('',(0.248000000194874,-0.744000000196067,1.2));
#16766=CARTESIAN_POINT('Origin',(0.248000000193922,-0.248000000194471,1.2));
#16767=CARTESIAN_POINT('',(0.248000000195456,-1.04682989872316,1.10790668314425));
#16768=CARTESIAN_POINT('Origin',(0.248000000193446,4.75999652275667E-13,
-5.12965591734105));
#16769=CARTESIAN_POINT('',(0.248000000195353,-0.993500000024651,1.01553658903593));
#16770=CARTESIAN_POINT('Origin',(-1.10000000000019,0.248000000196221,1.2));
#16771=CARTESIAN_POINT('',(-1.04682989872296,0.248000000196221,1.10790668314426));
#16772=CARTESIAN_POINT('Origin',(7.17605422133295E-15,0.248000000196221,
-5.12965591734105));
#16773=CARTESIAN_POINT('',(-1.10000000000019,0.248000000196221,1.2));
#16774=CARTESIAN_POINT('Origin',(-1.10000000000019,-0.248000000195508,1.2));
#16775=CARTESIAN_POINT('',(-1.04942373620595,-1.28517341949389E-16,1.11239934145138));
#16776=CARTESIAN_POINT('Origin',(1.91582141081578,-5.36035544273609E-16,
-4.02355591008731));
#16777=CARTESIAN_POINT('',(-0.516876228118667,-0.124000000097755,0.19));
#16778=CARTESIAN_POINT('Origin',(1.91582141081578,-5.36035544273609E-16,
-4.02355591008731));
#16779=CARTESIAN_POINT('Origin',(-0.248000000196409,-1.09999999999961,1.2));
#16780=CARTESIAN_POINT('',(-0.24800000019626,-1.04682989872243,1.10790668314434));
#16781=CARTESIAN_POINT('Origin',(-0.248000000193338,6.92337424395539E-13,
-5.12965591734105));
#16782=CARTESIAN_POINT('',(-0.248000000196409,-1.09999999999954,1.19999999999987));
#16783=CARTESIAN_POINT('Origin',(0.248000000195558,-1.10000000000039,1.2));
#16784=CARTESIAN_POINT('Origin',(3.00794342650252E-12,1.91582141081592,
-4.02355591008723));
#16785=CARTESIAN_POINT('',(0.124000000097801,-0.516876228118675,0.19));
#16786=CARTESIAN_POINT('Origin',(-5.91193760612896E-14,-1.66533453693773E-15,
0.19));
#16787=CARTESIAN_POINT('Origin',(0.,0.,-0.1));
#16788=CARTESIAN_POINT('',(0.939230484541328,-1.15022560655515E-16,0.));
#16789=CARTESIAN_POINT('Origin',(0.,0.,0.));
#16790=CARTESIAN_POINT('',(0.839230484541328,-1.02776092664042E-16,-0.1));
#16791=CARTESIAN_POINT('Origin',(0.939230484541328,-1.15022560655515E-16,
-0.1));
#16792=CARTESIAN_POINT('Origin',(0.,0.,-0.1));
#16793=CARTESIAN_POINT('Origin',(-0.839230484541328,0.,-7.24797437703358E-18));
#16794=CARTESIAN_POINT('',(2.15,-2.63299061816681E-16,0.));
#16795=CARTESIAN_POINT('Origin',(0.,0.,0.));
#16796=CARTESIAN_POINT('Origin',(0.,0.,-0.0749999999999998));
#16797=CARTESIAN_POINT('',(0.839230484541328,-1.02776092664042E-16,-0.15));
#16798=CARTESIAN_POINT('Origin',(0.,0.,-0.15));
#16799=CARTESIAN_POINT('',(0.839230484541328,-1.02776092664042E-16,-0.0749999999999998));
#16800=CARTESIAN_POINT('Origin',(0.,0.,-0.45));
#16801=CARTESIAN_POINT('',(0.96675,-1.1839272930757E-16,-0.625909310648334));
#16802=CARTESIAN_POINT('Origin',(0.,0.,-0.625909310648334));
#16803=CARTESIAN_POINT('',(0.919615242270664,-1.12620386289389E-16,-0.45));
#16804=CARTESIAN_POINT('Origin',(0.,0.,-3.375));
#16805=CARTESIAN_POINT('',(0.96675,1.1839272930757E-16,-6.));
#16806=CARTESIAN_POINT('Origin',(0.,0.,-6.));
#16807=CARTESIAN_POINT('',(0.96675,-1.1839272930757E-16,-3.375));
#16808=CARTESIAN_POINT('Origin',(0.,0.,-6.));
#16809=CARTESIAN_POINT('Origin',(7.21644966006352E-15,0.,-5.12965591734105));
#16810=CARTESIAN_POINT('',(-2.07563463599418,0.,0.85));
#16811=CARTESIAN_POINT('Origin',(7.21644966006352E-15,0.,-5.12965591734105));
#16812=CARTESIAN_POINT('',(2.07563463599418,-2.54191931316966E-16,0.85));
#16813=CARTESIAN_POINT('Origin',(0.,0.,0.85));
#16814=CARTESIAN_POINT('Origin',(0.,0.,0.85));
#16815=CARTESIAN_POINT('Origin',(0.,0.,0.425));
#16816=CARTESIAN_POINT('',(2.11281731799709,-2.58745496566823E-16,0.425));
#17026=UNCERTAINTY_MEASURE_WITH_UNIT(LENGTH_MEASURE(0.01),#17043,
'DISTANCE_ACCURACY_VALUE',
'Maximum model space distance between geometric entities at asserted c
onnectivities');
#17028=UNCERTAINTY_MEASURE_WITH_UNIT(LENGTH_MEASURE(0.01),#17043,
'DISTANCE_ACCURACY_VALUE',
'Maximum model space distance between geometric entities at asserted c
onnectivities');
#17040=(
GEOMETRIC_REPRESENTATION_CONTEXT(3)
GLOBAL_UNCERTAINTY_ASSIGNED_CONTEXT((#17026))
GLOBAL_UNIT_ASSIGNED_CONTEXT((#17043,#17045,#17046))
REPRESENTATION_CONTEXT('','3D')
);
#17042=(
GEOMETRIC_REPRESENTATION_CONTEXT(3)
GLOBAL_UNCERTAINTY_ASSIGNED_CONTEXT((#17028))
GLOBAL_UNIT_ASSIGNED_CONTEXT((#17043,#17045,#17046))
REPRESENTATION_CONTEXT('','3D')
);
#17043=(
LENGTH_UNIT()
NAMED_UNIT(*)
SI_UNIT(.MILLI.,.METRE.)
);
#17045=(
NAMED_UNIT(*)
PLANE_ANGLE_UNIT()
SI_UNIT($,.RADIAN.)
);
#17046=(
NAMED_UNIT(*)
SI_UNIT($,.STERADIAN.)
SOLID_ANGLE_UNIT()
);
#17058=SHAPE_DEFINITION_REPRESENTATION(#17071,#17096);
#17071=PRODUCT_DEFINITION_SHAPE('',$,#17110);
#17096=SHAPE_REPRESENTATION('',(#9117),#17040);
#17098=PRODUCT_DEFINITION_CONTEXT('part definition',#17139,'design');
#17110=PRODUCT_DEFINITION('BHS JIS B 1111 - M2x6 Steel 4.6 Plain_2',
'Binding Head Screw JIS B 1111 - M2x6 Steel 4.6 Plain v1 (3)',#17123,#17098);
#17123=PRODUCT_DEFINITION_FORMATION('',$,#17152);
#17139=APPLICATION_CONTEXT(
'Core Data for Automotive Mechanical Design Process');
#17140=PRODUCT_CONTEXT('part definition',#17139,'mechanical');
#17152=PRODUCT('BHS JIS B 1111 - M2x6 Steel 4.6 Plain_2',
'Binding Head Screw JIS B 1111 - M2x6 Steel 4.6 Plain v1 (3)',
'Binding Head Screw JIS B 1111 - M2x6',(#17140));
#17154=PRESENTATION_STYLE_ASSIGNMENT((#17155));
#17155=SURFACE_STYLE_USAGE(.BOTH.,#17156);
#17156=SURFACE_SIDE_STYLE('',(#17157));
#17157=SURFACE_STYLE_FILL_AREA(#17158);
#17158=FILL_AREA_STYLE('Steel - Satin',(#17159));
#17159=FILL_AREA_STYLE_COLOUR('Steel - Satin',#17160);
#17160=COLOUR_RGB('Steel - Satin', 0.09019608, 0.27058824, 0.51372549);
ENDSEC;
END-ISO-10303-21;
